ISO-10303-21;
HEADER;
/* Generated by software containing ST-Developer
 * from STEP Tools, Inc. (www.steptools.com) 
 */

FILE_DESCRIPTION(
/* description */ ('Five-roller gravity conveyor'),
/* implementation_level */ '2;1');

FILE_NAME(
/* name */ 'Axle Mount B.step',
/* time_stamp */ '2026-10-29T15:36:43-07:00',
/* author */ (''),
/* organization */ (''),
/* preprocessor_version */ 'ST-DEVELOPER v20.2',
/* originating_system */ 'Autodesk Translation Framework v15.17.0.0',
/* authorisation */ '');

FILE_SCHEMA (('AUTOMOTIVE_DESIGN { 1 0 10303 214 3 1 1 }'));
ENDSEC;

DATA;
#10=MECHANICAL_DESIGN_GEOMETRIC_PRESENTATION_REPRESENTATION('',(#315),#7806);
#279=SHAPE_REPRESENTATION_RELATIONSHIP('SRR','None',#7916,#297);
#297=ADVANCED_BREP_SHAPE_REPRESENTATION('',(#341),#7789);
#315=STYLED_ITEM('',(#8091),#341);
#341=MANIFOLD_SOLID_BREP('Body1',#4202);
#374=FACE_BOUND('',#978,.T.);
#375=FACE_BOUND('',#982,.T.);
#376=FACE_BOUND('',#984,.T.);
#377=FACE_BOUND('',#996,.T.);
#378=FACE_BOUND('',#1000,.T.);
#379=FACE_BOUND('',#1001,.T.);
#447=CIRCLE('',#4539,0.5);
#448=CIRCLE('',#4540,0.5);
#449=CIRCLE('',#4542,0.5);
#450=CIRCLE('',#4543,0.5);
#451=CIRCLE('',#4545,0.275);
#452=CIRCLE('',#4547,0.5);
#453=CIRCLE('',#4548,0.5);
#454=CIRCLE('',#4550,0.5);
#455=CIRCLE('',#4551,0.5);
#456=CIRCLE('',#4553,0.275);
#457=CIRCLE('',#4555,0.505);
#458=CIRCLE('',#4560,0.275);
#459=CIRCLE('',#4562,0.275);
#460=CIRCLE('',#4564,0.505);
#607=CYLINDRICAL_SURFACE('',#4538,0.5);
#608=CYLINDRICAL_SURFACE('',#4541,0.5);
#609=CYLINDRICAL_SURFACE('',#4546,0.5);
#610=CYLINDRICAL_SURFACE('',#4549,0.5);
#611=CYLINDRICAL_SURFACE('',#4559,0.275);
#612=CYLINDRICAL_SURFACE('',#4561,0.275);
#613=CYLINDRICAL_SURFACE('',#4563,0.505);
#731=FACE_OUTER_BOUND('',#975,.T.);
#732=FACE_OUTER_BOUND('',#976,.T.);
#733=FACE_OUTER_BOUND('',#977,.T.);
#734=FACE_OUTER_BOUND('',#979,.T.);
#735=FACE_OUTER_BOUND('',#980,.T.);
#736=FACE_OUTER_BOUND('',#981,.T.);
#737=FACE_OUTER_BOUND('',#983,.T.);
#738=FACE_OUTER_BOUND('',#985,.T.);
#739=FACE_OUTER_BOUND('',#986,.T.);
#740=FACE_OUTER_BOUND('',#987,.T.);
#741=FACE_OUTER_BOUND('',#988,.T.);
#742=FACE_OUTER_BOUND('',#989,.T.);
#743=FACE_OUTER_BOUND('',#990,.T.);
#744=FACE_OUTER_BOUND('',#991,.T.);
#745=FACE_OUTER_BOUND('',#992,.T.);
#746=FACE_OUTER_BOUND('',#993,.T.);
#747=FACE_OUTER_BOUND('',#994,.T.);
#748=FACE_OUTER_BOUND('',#995,.T.);
#749=FACE_OUTER_BOUND('',#997,.T.);
#750=FACE_OUTER_BOUND('',#998,.T.);
#751=FACE_OUTER_BOUND('',#999,.T.);
#975=EDGE_LOOP('',(#3168,#3169,#3170,#3171));
#976=EDGE_LOOP('',(#3172,#3173,#3174,#3175));
#977=EDGE_LOOP('',(#3176,#3177,#3178,#3179));
#978=EDGE_LOOP('',(#3180));
#979=EDGE_LOOP('',(#3181,#3182,#3183,#3184));
#980=EDGE_LOOP('',(#3185,#3186,#3187,#3188));
#981=EDGE_LOOP('',(#3189,#3190,#3191,#3192));
#982=EDGE_LOOP('',(#3193));
#983=EDGE_LOOP('',(#3194,#3195,#3196,#3197,#3198,#3199,#3200,#3201,#3202,
#3203,#3204,#3205));
#984=EDGE_LOOP('',(#3206));
#985=EDGE_LOOP('',(#3207,#3208,#3209,#3210));
#986=EDGE_LOOP('',(#3211,#3212,#3213,#3214));
#987=EDGE_LOOP('',(#3215,#3216,#3217,#3218));
#988=EDGE_LOOP('',(#3219,#3220,#3221,#3222));
#989=EDGE_LOOP('',(#3223,#3224,#3225,#3226));
#990=EDGE_LOOP('',(#3227,#3228,#3229,#3230));
#991=EDGE_LOOP('',(#3231,#3232,#3233,#3234));
#992=EDGE_LOOP('',(#3235,#3236,#3237,#3238));
#993=EDGE_LOOP('',(#3239,#3240,#3241,#3242));
#994=EDGE_LOOP('',(#3243,#3244,#3245,#3246));
#995=EDGE_LOOP('',(#3247,#3248,#3249,#3250,#3251,#3252,#3253,#3254,#3255,
#3256,#3257,#3258));
#996=EDGE_LOOP('',(#3259));
#997=EDGE_LOOP('',(#3260,#3261,#3262,#3263,#3264,#3265,#3266,#3267));
#998=EDGE_LOOP('',(#3268,#3269,#3270,#3271,#3272,#3273,#3274,#3275));
#999=EDGE_LOOP('',(#3276,#3277,#3278,#3279));
#1000=EDGE_LOOP('',(#3280));
#1001=EDGE_LOOP('',(#3281));
#1356=LINE('',#6650,#1697);
#1357=LINE('',#6654,#1698);
#1358=LINE('',#6659,#1699);
#1359=LINE('',#6663,#1700);
#1360=LINE('',#6666,#1701);
#1361=LINE('',#6667,#1702);
#1362=LINE('',#6673,#1703);
#1363=LINE('',#6677,#1704);
#1364=LINE('',#6682,#1705);
#1365=LINE('',#6686,#1706);
#1366=LINE('',#6689,#1707);
#1367=LINE('',#6690,#1708);
#1368=LINE('',#6695,#1709);
#1369=LINE('',#6697,#1710);
#1370=LINE('',#6699,#1711);
#1371=LINE('',#6701,#1712);
#1372=LINE('',#6702,#1713);
#1373=LINE('',#6703,#1714);
#1374=LINE('',#6708,#1715);
#1375=LINE('',#6709,#1716);
#1376=LINE('',#6712,#1717);
#1377=LINE('',#6713,#1718);
#1378=LINE('',#6715,#1719);
#1379=LINE('',#6719,#1720);
#1380=LINE('',#6723,#1721);
#1381=LINE('',#6726,#1722);
#1382=LINE('',#6730,#1723);
#1383=LINE('',#6732,#1724);
#1384=LINE('',#6733,#1725);
#1385=LINE('',#6737,#1726);
#1386=LINE('',#6739,#1727);
#1387=LINE('',#6741,#1728);
#1388=LINE('',#6742,#1729);
#1389=LINE('',#6745,#1730);
#1390=LINE('',#6747,#1731);
#1391=LINE('',#6748,#1732);
#1392=LINE('',#6751,#1733);
#1393=LINE('',#6753,#1734);
#1394=LINE('',#6754,#1735);
#1395=LINE('',#6756,#1736);
#1396=LINE('',#6757,#1737);
#1397=LINE('',#6759,#1738);
#1398=LINE('',#6761,#1739);
#1697=VECTOR('',#5316,1.);
#1698=VECTOR('',#5319,1.);
#1699=VECTOR('',#5324,1.);
#1700=VECTOR('',#5327,1.);
#1701=VECTOR('',#5332,1.);
#1702=VECTOR('',#5333,1.);
#1703=VECTOR('',#5338,1.);
#1704=VECTOR('',#5341,1.);
#1705=VECTOR('',#5346,1.);
#1706=VECTOR('',#5349,1.);
#1707=VECTOR('',#5354,1.);
#1708=VECTOR('',#5355,1.);
#1709=VECTOR('',#5360,1.);
#1710=VECTOR('',#5361,1.);
#1711=VECTOR('',#5362,1.);
#1712=VECTOR('',#5363,1.);
#1713=VECTOR('',#5364,1.);
#1714=VECTOR('',#5365,1.);
#1715=VECTOR('',#5370,1.);
#1716=VECTOR('',#5371,1.);
#1717=VECTOR('',#5374,1.);
#1718=VECTOR('',#5375,1.);
#1719=VECTOR('',#5378,1.);
#1720=VECTOR('',#5383,0.275);
#1721=VECTOR('',#5388,0.275);
#1722=VECTOR('',#5391,0.505);
#1723=VECTOR('',#5396,1.);
#1724=VECTOR('',#5397,1.);
#1725=VECTOR('',#5398,1.);
#1726=VECTOR('',#5401,1.);
#1727=VECTOR('',#5402,1.);
#1728=VECTOR('',#5403,1.);
#1729=VECTOR('',#5404,1.);
#1730=VECTOR('',#5407,1.);
#1731=VECTOR('',#5408,1.);
#1732=VECTOR('',#5409,1.);
#1733=VECTOR('',#5412,1.);
#1734=VECTOR('',#5413,1.);
#1735=VECTOR('',#5414,1.);
#1736=VECTOR('',#5417,1.);
#1737=VECTOR('',#5418,1.);
#1738=VECTOR('',#5421,1.);
#1739=VECTOR('',#5424,1.);
#1995=VERTEX_POINT('',#6648);
#1996=VERTEX_POINT('',#6649);
#1997=VERTEX_POINT('',#6651);
#1998=VERTEX_POINT('',#6653);
#1999=VERTEX_POINT('',#6657);
#2000=VERTEX_POINT('',#6658);
#2001=VERTEX_POINT('',#6660);
#2002=VERTEX_POINT('',#6662);
#2003=VERTEX_POINT('',#6668);
#2004=VERTEX_POINT('',#6671);
#2005=VERTEX_POINT('',#6672);
#2006=VERTEX_POINT('',#6674);
#2007=VERTEX_POINT('',#6676);
#2008=VERTEX_POINT('',#6680);
#2009=VERTEX_POINT('',#6681);
#2010=VERTEX_POINT('',#6683);
#2011=VERTEX_POINT('',#6685);
#2012=VERTEX_POINT('',#6691);
#2013=VERTEX_POINT('',#6694);
#2014=VERTEX_POINT('',#6696);
#2015=VERTEX_POINT('',#6698);
#2016=VERTEX_POINT('',#6700);
#2017=VERTEX_POINT('',#6704);
#2018=VERTEX_POINT('',#6707);
#2019=VERTEX_POINT('',#6711);
#2020=VERTEX_POINT('',#6717);
#2021=VERTEX_POINT('',#6721);
#2022=VERTEX_POINT('',#6725);
#2023=VERTEX_POINT('',#6729);
#2024=VERTEX_POINT('',#6731);
#2025=VERTEX_POINT('',#6735);
#2026=VERTEX_POINT('',#6736);
#2027=VERTEX_POINT('',#6738);
#2028=VERTEX_POINT('',#6740);
#2029=VERTEX_POINT('',#6744);
#2030=VERTEX_POINT('',#6746);
#2031=VERTEX_POINT('',#6750);
#2032=VERTEX_POINT('',#6752);
#2427=EDGE_CURVE('',#1995,#1996,#1356,.T.);
#2428=EDGE_CURVE('',#1997,#1995,#447,.T.);
#2429=EDGE_CURVE('',#1998,#1997,#1357,.T.);
#2430=EDGE_CURVE('',#1996,#1998,#448,.T.);
#2431=EDGE_CURVE('',#1999,#2000,#1358,.T.);
#2432=EDGE_CURVE('',#2001,#1999,#449,.T.);
#2433=EDGE_CURVE('',#2002,#2001,#1359,.T.);
#2434=EDGE_CURVE('',#2000,#2002,#450,.T.);
#2435=EDGE_CURVE('',#1996,#1999,#1360,.T.);
#2436=EDGE_CURVE('',#2001,#1998,#1361,.T.);
#2437=EDGE_CURVE('',#2003,#2003,#451,.T.);
#2438=EDGE_CURVE('',#2004,#2005,#1362,.T.);
#2439=EDGE_CURVE('',#2006,#2004,#452,.T.);
#2440=EDGE_CURVE('',#2007,#2006,#1363,.T.);
#2441=EDGE_CURVE('',#2005,#2007,#453,.T.);
#2442=EDGE_CURVE('',#2008,#2009,#1364,.T.);
#2443=EDGE_CURVE('',#2010,#2008,#454,.T.);
#2444=EDGE_CURVE('',#2011,#2010,#1365,.T.);
#2445=EDGE_CURVE('',#2009,#2011,#455,.T.);
#2446=EDGE_CURVE('',#2005,#2008,#1366,.T.);
#2447=EDGE_CURVE('',#2010,#2007,#1367,.T.);
#2448=EDGE_CURVE('',#2012,#2012,#456,.T.);
#2449=EDGE_CURVE('',#2013,#1997,#1368,.T.);
#2450=EDGE_CURVE('',#2014,#2013,#1369,.T.);
#2451=EDGE_CURVE('',#2014,#2015,#1370,.T.);
#2452=EDGE_CURVE('',#2015,#2016,#1371,.T.);
#2453=EDGE_CURVE('',#2011,#2016,#1372,.T.);
#2454=EDGE_CURVE('',#2002,#2006,#1373,.T.);
#2455=EDGE_CURVE('',#2017,#2017,#457,.T.);
#2456=EDGE_CURVE('',#2016,#2018,#1374,.T.);
#2457=EDGE_CURVE('',#2018,#2009,#1375,.T.);
#2458=EDGE_CURVE('',#1995,#2019,#1376,.T.);
#2459=EDGE_CURVE('',#2019,#2013,#1377,.T.);
#2460=EDGE_CURVE('',#2004,#2000,#1378,.T.);
#2461=EDGE_CURVE('',#2020,#2020,#458,.T.);
#2462=EDGE_CURVE('',#2020,#2003,#1379,.T.);
#2463=EDGE_CURVE('',#2021,#2021,#459,.T.);
#2464=EDGE_CURVE('',#2021,#2012,#1380,.T.);
#2465=EDGE_CURVE('',#2017,#2022,#1381,.T.);
#2466=EDGE_CURVE('',#2022,#2022,#460,.T.);
#2467=EDGE_CURVE('',#2023,#2014,#1382,.T.);
#2468=EDGE_CURVE('',#2024,#2023,#1383,.T.);
#2469=EDGE_CURVE('',#2024,#2015,#1384,.T.);
#2470=EDGE_CURVE('',#2025,#2026,#1385,.T.);
#2471=EDGE_CURVE('',#2025,#2027,#1386,.T.);
#2472=EDGE_CURVE('',#2028,#2027,#1387,.T.);
#2473=EDGE_CURVE('',#2026,#2028,#1388,.T.);
#2474=EDGE_CURVE('',#2027,#2029,#1389,.T.);
#2475=EDGE_CURVE('',#2029,#2030,#1390,.T.);
#2476=EDGE_CURVE('',#2030,#2028,#1391,.T.);
#2477=EDGE_CURVE('',#2023,#2031,#1392,.T.);
#2478=EDGE_CURVE('',#2031,#2032,#1393,.T.);
#2479=EDGE_CURVE('',#2032,#2024,#1394,.T.);
#2480=EDGE_CURVE('',#2025,#2018,#1395,.T.);
#2481=EDGE_CURVE('',#2026,#2019,#1396,.T.);
#2482=EDGE_CURVE('',#2030,#2031,#1397,.T.);
#2483=EDGE_CURVE('',#2032,#2029,#1398,.T.);
#3168=ORIENTED_EDGE('',*,*,#2427,.F.);
#3169=ORIENTED_EDGE('',*,*,#2428,.F.);
#3170=ORIENTED_EDGE('',*,*,#2429,.F.);
#3171=ORIENTED_EDGE('',*,*,#2430,.F.);
#3172=ORIENTED_EDGE('',*,*,#2431,.F.);
#3173=ORIENTED_EDGE('',*,*,#2432,.F.);
#3174=ORIENTED_EDGE('',*,*,#2433,.F.);
#3175=ORIENTED_EDGE('',*,*,#2434,.F.);
#3176=ORIENTED_EDGE('',*,*,#2435,.F.);
#3177=ORIENTED_EDGE('',*,*,#2430,.T.);
#3178=ORIENTED_EDGE('',*,*,#2436,.F.);
#3179=ORIENTED_EDGE('',*,*,#2432,.T.);
#3180=ORIENTED_EDGE('',*,*,#2437,.F.);
#3181=ORIENTED_EDGE('',*,*,#2438,.F.);
#3182=ORIENTED_EDGE('',*,*,#2439,.F.);
#3183=ORIENTED_EDGE('',*,*,#2440,.F.);
#3184=ORIENTED_EDGE('',*,*,#2441,.F.);
#3185=ORIENTED_EDGE('',*,*,#2442,.F.);
#3186=ORIENTED_EDGE('',*,*,#2443,.F.);
#3187=ORIENTED_EDGE('',*,*,#2444,.F.);
#3188=ORIENTED_EDGE('',*,*,#2445,.F.);
#3189=ORIENTED_EDGE('',*,*,#2446,.F.);
#3190=ORIENTED_EDGE('',*,*,#2441,.T.);
#3191=ORIENTED_EDGE('',*,*,#2447,.F.);
#3192=ORIENTED_EDGE('',*,*,#2443,.T.);
#3193=ORIENTED_EDGE('',*,*,#2448,.F.);
#3194=ORIENTED_EDGE('',*,*,#2433,.T.);
#3195=ORIENTED_EDGE('',*,*,#2436,.T.);
#3196=ORIENTED_EDGE('',*,*,#2429,.T.);
#3197=ORIENTED_EDGE('',*,*,#2449,.F.);
#3198=ORIENTED_EDGE('',*,*,#2450,.F.);
#3199=ORIENTED_EDGE('',*,*,#2451,.T.);
#3200=ORIENTED_EDGE('',*,*,#2452,.T.);
#3201=ORIENTED_EDGE('',*,*,#2453,.F.);
#3202=ORIENTED_EDGE('',*,*,#2444,.T.);
#3203=ORIENTED_EDGE('',*,*,#2447,.T.);
#3204=ORIENTED_EDGE('',*,*,#2440,.T.);
#3205=ORIENTED_EDGE('',*,*,#2454,.F.);
#3206=ORIENTED_EDGE('',*,*,#2455,.T.);
#3207=ORIENTED_EDGE('',*,*,#2445,.T.);
#3208=ORIENTED_EDGE('',*,*,#2453,.T.);
#3209=ORIENTED_EDGE('',*,*,#2456,.T.);
#3210=ORIENTED_EDGE('',*,*,#2457,.T.);
#3211=ORIENTED_EDGE('',*,*,#2428,.T.);
#3212=ORIENTED_EDGE('',*,*,#2458,.T.);
#3213=ORIENTED_EDGE('',*,*,#2459,.T.);
#3214=ORIENTED_EDGE('',*,*,#2449,.T.);
#3215=ORIENTED_EDGE('',*,*,#2434,.T.);
#3216=ORIENTED_EDGE('',*,*,#2454,.T.);
#3217=ORIENTED_EDGE('',*,*,#2439,.T.);
#3218=ORIENTED_EDGE('',*,*,#2460,.T.);
#3219=ORIENTED_EDGE('',*,*,#2461,.F.);
#3220=ORIENTED_EDGE('',*,*,#2462,.T.);
#3221=ORIENTED_EDGE('',*,*,#2437,.T.);
#3222=ORIENTED_EDGE('',*,*,#2462,.F.);
#3223=ORIENTED_EDGE('',*,*,#2463,.F.);
#3224=ORIENTED_EDGE('',*,*,#2464,.T.);
#3225=ORIENTED_EDGE('',*,*,#2448,.T.);
#3226=ORIENTED_EDGE('',*,*,#2464,.F.);
#3227=ORIENTED_EDGE('',*,*,#2455,.F.);
#3228=ORIENTED_EDGE('',*,*,#2465,.T.);
#3229=ORIENTED_EDGE('',*,*,#2466,.F.);
#3230=ORIENTED_EDGE('',*,*,#2465,.F.);
#3231=ORIENTED_EDGE('',*,*,#2451,.F.);
#3232=ORIENTED_EDGE('',*,*,#2467,.F.);
#3233=ORIENTED_EDGE('',*,*,#2468,.F.);
#3234=ORIENTED_EDGE('',*,*,#2469,.T.);
#3235=ORIENTED_EDGE('',*,*,#2470,.F.);
#3236=ORIENTED_EDGE('',*,*,#2471,.T.);
#3237=ORIENTED_EDGE('',*,*,#2472,.F.);
#3238=ORIENTED_EDGE('',*,*,#2473,.F.);
#3239=ORIENTED_EDGE('',*,*,#2472,.T.);
#3240=ORIENTED_EDGE('',*,*,#2474,.T.);
#3241=ORIENTED_EDGE('',*,*,#2475,.T.);
#3242=ORIENTED_EDGE('',*,*,#2476,.T.);
#3243=ORIENTED_EDGE('',*,*,#2468,.T.);
#3244=ORIENTED_EDGE('',*,*,#2477,.T.);
#3245=ORIENTED_EDGE('',*,*,#2478,.T.);
#3246=ORIENTED_EDGE('',*,*,#2479,.T.);
#3247=ORIENTED_EDGE('',*,*,#2431,.T.);
#3248=ORIENTED_EDGE('',*,*,#2460,.F.);
#3249=ORIENTED_EDGE('',*,*,#2438,.T.);
#3250=ORIENTED_EDGE('',*,*,#2446,.T.);
#3251=ORIENTED_EDGE('',*,*,#2442,.T.);
#3252=ORIENTED_EDGE('',*,*,#2457,.F.);
#3253=ORIENTED_EDGE('',*,*,#2480,.F.);
#3254=ORIENTED_EDGE('',*,*,#2470,.T.);
#3255=ORIENTED_EDGE('',*,*,#2481,.T.);
#3256=ORIENTED_EDGE('',*,*,#2458,.F.);
#3257=ORIENTED_EDGE('',*,*,#2427,.T.);
#3258=ORIENTED_EDGE('',*,*,#2435,.T.);
#3259=ORIENTED_EDGE('',*,*,#2466,.T.);
#3260=ORIENTED_EDGE('',*,*,#2450,.T.);
#3261=ORIENTED_EDGE('',*,*,#2459,.F.);
#3262=ORIENTED_EDGE('',*,*,#2481,.F.);
#3263=ORIENTED_EDGE('',*,*,#2473,.T.);
#3264=ORIENTED_EDGE('',*,*,#2476,.F.);
#3265=ORIENTED_EDGE('',*,*,#2482,.T.);
#3266=ORIENTED_EDGE('',*,*,#2477,.F.);
#3267=ORIENTED_EDGE('',*,*,#2467,.T.);
#3268=ORIENTED_EDGE('',*,*,#2480,.T.);
#3269=ORIENTED_EDGE('',*,*,#2456,.F.);
#3270=ORIENTED_EDGE('',*,*,#2452,.F.);
#3271=ORIENTED_EDGE('',*,*,#2469,.F.);
#3272=ORIENTED_EDGE('',*,*,#2479,.F.);
#3273=ORIENTED_EDGE('',*,*,#2483,.T.);
#3274=ORIENTED_EDGE('',*,*,#2474,.F.);
#3275=ORIENTED_EDGE('',*,*,#2471,.F.);
#3276=ORIENTED_EDGE('',*,*,#2482,.F.);
#3277=ORIENTED_EDGE('',*,*,#2475,.F.);
#3278=ORIENTED_EDGE('',*,*,#2483,.F.);
#3279=ORIENTED_EDGE('',*,*,#2478,.F.);
#3280=ORIENTED_EDGE('',*,*,#2461,.T.);
#3281=ORIENTED_EDGE('',*,*,#2463,.T.);
#3888=PLANE('',#4544);
#3889=PLANE('',#4552);
#3890=PLANE('',#4554);
#3891=PLANE('',#4556);
#3892=PLANE('',#4557);
#3893=PLANE('',#4558);
#3894=PLANE('',#4565);
#3895=PLANE('',#4566);
#3896=PLANE('',#4567);
#3897=PLANE('',#4568);
#3898=PLANE('',#4569);
#3899=PLANE('',#4570);
#3900=PLANE('',#4571);
#3901=PLANE('',#4572);
#4046=ADVANCED_FACE('',(#731),#607,.F.);
#4047=ADVANCED_FACE('',(#732),#608,.F.);
#4048=ADVANCED_FACE('',(#733,#374),#3888,.T.);
#4049=ADVANCED_FACE('',(#734),#609,.F.);
#4050=ADVANCED_FACE('',(#735),#610,.F.);
#4051=ADVANCED_FACE('',(#736,#375),#3889,.T.);
#4052=ADVANCED_FACE('',(#737,#376),#3890,.T.);
#4053=ADVANCED_FACE('',(#738),#3891,.T.);
#4054=ADVANCED_FACE('',(#739),#3892,.T.);
#4055=ADVANCED_FACE('',(#740),#3893,.T.);
#4056=ADVANCED_FACE('',(#741),#611,.F.);
#4057=ADVANCED_FACE('',(#742),#612,.F.);
#4058=ADVANCED_FACE('',(#743),#613,.F.);
#4059=ADVANCED_FACE('',(#744),#3894,.T.);
#4060=ADVANCED_FACE('',(#745),#3895,.T.);
#4061=ADVANCED_FACE('',(#746),#3896,.T.);
#4062=ADVANCED_FACE('',(#747),#3897,.F.);
#4063=ADVANCED_FACE('',(#748,#377),#3898,.T.);
#4064=ADVANCED_FACE('',(#749),#3899,.T.);
#4065=ADVANCED_FACE('',(#750),#3900,.T.);
#4066=ADVANCED_FACE('',(#751,#378,#379),#3901,.F.);
#4202=CLOSED_SHELL('',(#4046,#4047,#4048,#4049,#4050,#4051,#4052,#4053,
#4054,#4055,#4056,#4057,#4058,#4059,#4060,#4061,#4062,#4063,#4064,#4065,
#4066));
#4537=AXIS2_PLACEMENT_3D('',#6646,#5312,#5313);
#4538=AXIS2_PLACEMENT_3D('',#6647,#5314,#5315);
#4539=AXIS2_PLACEMENT_3D('',#6652,#5317,#5318);
#4540=AXIS2_PLACEMENT_3D('',#6655,#5320,#5321);
#4541=AXIS2_PLACEMENT_3D('',#6656,#5322,#5323);
#4542=AXIS2_PLACEMENT_3D('',#6661,#5325,#5326);
#4543=AXIS2_PLACEMENT_3D('',#6664,#5328,#5329);
#4544=AXIS2_PLACEMENT_3D('',#6665,#5330,#5331);
#4545=AXIS2_PLACEMENT_3D('',#6669,#5334,#5335);
#4546=AXIS2_PLACEMENT_3D('',#6670,#5336,#5337);
#4547=AXIS2_PLACEMENT_3D('',#6675,#5339,#5340);
#4548=AXIS2_PLACEMENT_3D('',#6678,#5342,#5343);
#4549=AXIS2_PLACEMENT_3D('',#6679,#5344,#5345);
#4550=AXIS2_PLACEMENT_3D('',#6684,#5347,#5348);
#4551=AXIS2_PLACEMENT_3D('',#6687,#5350,#5351);
#4552=AXIS2_PLACEMENT_3D('',#6688,#5352,#5353);
#4553=AXIS2_PLACEMENT_3D('',#6692,#5356,#5357);
#4554=AXIS2_PLACEMENT_3D('',#6693,#5358,#5359);
#4555=AXIS2_PLACEMENT_3D('',#6705,#5366,#5367);
#4556=AXIS2_PLACEMENT_3D('',#6706,#5368,#5369);
#4557=AXIS2_PLACEMENT_3D('',#6710,#5372,#5373);
#4558=AXIS2_PLACEMENT_3D('',#6714,#5376,#5377);
#4559=AXIS2_PLACEMENT_3D('',#6716,#5379,#5380);
#4560=AXIS2_PLACEMENT_3D('',#6718,#5381,#5382);
#4561=AXIS2_PLACEMENT_3D('',#6720,#5384,#5385);
#4562=AXIS2_PLACEMENT_3D('',#6722,#5386,#5387);
#4563=AXIS2_PLACEMENT_3D('',#6724,#5389,#5390);
#4564=AXIS2_PLACEMENT_3D('',#6727,#5392,#5393);
#4565=AXIS2_PLACEMENT_3D('',#6728,#5394,#5395);
#4566=AXIS2_PLACEMENT_3D('',#6734,#5399,#5400);
#4567=AXIS2_PLACEMENT_3D('',#6743,#5405,#5406);
#4568=AXIS2_PLACEMENT_3D('',#6749,#5410,#5411);
#4569=AXIS2_PLACEMENT_3D('',#6755,#5415,#5416);
#4570=AXIS2_PLACEMENT_3D('',#6758,#5419,#5420);
#4571=AXIS2_PLACEMENT_3D('',#6760,#5422,#5423);
#4572=AXIS2_PLACEMENT_3D('',#6762,#5425,#5426);
#5312=DIRECTION('axis',(0.,0.,1.));
#5313=DIRECTION('refdir',(1.,0.,0.));
#5314=DIRECTION('center_axis',(0.,0.,1.));
#5315=DIRECTION('ref_axis',(-1.,1.22464679914735E-16,0.));
#5316=DIRECTION('',(0.,0.,-1.));
#5317=DIRECTION('center_axis',(0.,0.,-1.));
#5318=DIRECTION('ref_axis',(1.,0.,0.));
#5319=DIRECTION('',(0.,0.,1.));
#5320=DIRECTION('center_axis',(0.,0.,1.));
#5321=DIRECTION('ref_axis',(1.,0.,0.));
#5322=DIRECTION('center_axis',(0.,0.,1.));
#5323=DIRECTION('ref_axis',(1.,0.,0.));
#5324=DIRECTION('',(0.,0.,1.));
#5325=DIRECTION('center_axis',(0.,0.,1.));
#5326=DIRECTION('ref_axis',(1.,0.,0.));
#5327=DIRECTION('',(0.,0.,-1.));
#5328=DIRECTION('center_axis',(0.,0.,-1.));
#5329=DIRECTION('ref_axis',(1.,0.,0.));
#5330=DIRECTION('center_axis',(0.,0.,1.));
#5331=DIRECTION('ref_axis',(1.,0.,0.));
#5332=DIRECTION('',(1.,0.,0.));
#5333=DIRECTION('',(-1.,0.,0.));
#5334=DIRECTION('center_axis',(0.,0.,1.));
#5335=DIRECTION('ref_axis',(1.,0.,0.));
#5336=DIRECTION('center_axis',(0.,0.,1.));
#5337=DIRECTION('ref_axis',(-1.,1.22464679914735E-16,0.));
#5338=DIRECTION('',(0.,0.,-1.));
#5339=DIRECTION('center_axis',(0.,0.,-1.));
#5340=DIRECTION('ref_axis',(1.,0.,0.));
#5341=DIRECTION('',(0.,0.,1.));
#5342=DIRECTION('center_axis',(0.,0.,1.));
#5343=DIRECTION('ref_axis',(1.,0.,0.));
#5344=DIRECTION('center_axis',(0.,0.,1.));
#5345=DIRECTION('ref_axis',(1.,0.,0.));
#5346=DIRECTION('',(0.,0.,1.));
#5347=DIRECTION('center_axis',(0.,0.,1.));
#5348=DIRECTION('ref_axis',(1.,0.,0.));
#5349=DIRECTION('',(0.,0.,-1.));
#5350=DIRECTION('center_axis',(0.,0.,-1.));
#5351=DIRECTION('ref_axis',(1.,0.,0.));
#5352=DIRECTION('center_axis',(0.,0.,1.));
#5353=DIRECTION('ref_axis',(1.,0.,0.));
#5354=DIRECTION('',(1.,0.,0.));
#5355=DIRECTION('',(-1.,0.,0.));
#5356=DIRECTION('center_axis',(0.,0.,1.));
#5357=DIRECTION('ref_axis',(1.,0.,0.));
#5358=DIRECTION('center_axis',(0.,-1.,0.));
#5359=DIRECTION('ref_axis',(1.,0.,0.));
#5360=DIRECTION('',(1.,0.,0.));
#5361=DIRECTION('',(0.,0.,1.));
#5362=DIRECTION('',(1.,0.,0.));
#5363=DIRECTION('',(0.,0.,1.));
#5364=DIRECTION('',(1.,0.,0.));
#5365=DIRECTION('',(1.,0.,0.));
#5366=DIRECTION('center_axis',(0.,1.,0.));
#5367=DIRECTION('ref_axis',(1.,0.,0.));
#5368=DIRECTION('center_axis',(0.,0.,1.));
#5369=DIRECTION('ref_axis',(1.,0.,0.));
#5370=DIRECTION('',(0.,1.,0.));
#5371=DIRECTION('',(-1.,0.,0.));
#5372=DIRECTION('center_axis',(0.,0.,1.));
#5373=DIRECTION('ref_axis',(1.,0.,0.));
#5374=DIRECTION('',(-1.,0.,0.));
#5375=DIRECTION('',(0.,-1.,0.));
#5376=DIRECTION('center_axis',(0.,0.,1.));
#5377=DIRECTION('ref_axis',(1.,0.,0.));
#5378=DIRECTION('',(-1.,0.,0.));
#5379=DIRECTION('center_axis',(0.,0.,1.));
#5380=DIRECTION('ref_axis',(1.,0.,0.));
#5381=DIRECTION('center_axis',(0.,0.,1.));
#5382=DIRECTION('ref_axis',(1.,0.,0.));
#5383=DIRECTION('',(0.,0.,1.));
#5384=DIRECTION('center_axis',(0.,0.,1.));
#5385=DIRECTION('ref_axis',(1.,0.,0.));
#5386=DIRECTION('center_axis',(0.,0.,1.));
#5387=DIRECTION('ref_axis',(1.,0.,0.));
#5388=DIRECTION('',(0.,0.,1.));
#5389=DIRECTION('center_axis',(0.,1.,0.));
#5390=DIRECTION('ref_axis',(1.,0.,0.));
#5391=DIRECTION('',(0.,1.,0.));
#5392=DIRECTION('center_axis',(0.,-1.,0.));
#5393=DIRECTION('ref_axis',(1.,0.,0.));
#5394=DIRECTION('center_axis',(0.,0.,1.));
#5395=DIRECTION('ref_axis',(1.,0.,0.));
#5396=DIRECTION('',(0.,1.,0.));
#5397=DIRECTION('',(-1.,0.,0.));
#5398=DIRECTION('',(0.,1.,0.));
#5399=DIRECTION('center_axis',(0.,0.,1.));
#5400=DIRECTION('ref_axis',(1.,0.,0.));
#5401=DIRECTION('',(-1.,0.,0.));
#5402=DIRECTION('',(0.,1.,0.));
#5403=DIRECTION('',(1.,0.,0.));
#5404=DIRECTION('',(0.,1.,0.));
#5405=DIRECTION('center_axis',(0.,1.,0.));
#5406=DIRECTION('ref_axis',(0.,0.,1.));
#5407=DIRECTION('',(0.,0.,-1.));
#5408=DIRECTION('',(-1.,0.,0.));
#5409=DIRECTION('',(0.,0.,1.));
#5410=DIRECTION('center_axis',(0.,1.,0.));
#5411=DIRECTION('ref_axis',(1.,0.,0.));
#5412=DIRECTION('',(0.,0.,-1.));
#5413=DIRECTION('',(1.,0.,0.));
#5414=DIRECTION('',(0.,0.,1.));
#5415=DIRECTION('center_axis',(0.,1.,0.));
#5416=DIRECTION('ref_axis',(-1.,0.,0.));
#5417=DIRECTION('',(0.,0.,1.));
#5418=DIRECTION('',(0.,0.,1.));
#5419=DIRECTION('center_axis',(-1.,0.,0.));
#5420=DIRECTION('ref_axis',(0.,-1.,0.));
#5421=DIRECTION('',(0.,-1.,0.));
#5422=DIRECTION('center_axis',(1.,0.,0.));
#5423=DIRECTION('ref_axis',(0.,1.,0.));
#5424=DIRECTION('',(0.,1.,0.));
#5425=DIRECTION('center_axis',(0.,0.,1.));
#5426=DIRECTION('ref_axis',(1.,0.,0.));
#6646=CARTESIAN_POINT('',(0.,0.,0.));
#6647=CARTESIAN_POINT('Origin',(1.6,32.,2.9));
#6648=CARTESIAN_POINT('',(1.3,32.4,6.5));
#6649=CARTESIAN_POINT('',(1.3,32.4,2.9));
#6650=CARTESIAN_POINT('',(1.3,32.4,2.9));
#6651=CARTESIAN_POINT('',(1.3,31.6,6.5));
#6652=CARTESIAN_POINT('Origin',(1.6,32.,6.5));
#6653=CARTESIAN_POINT('',(1.3,31.6,2.9));
#6654=CARTESIAN_POINT('',(1.3,31.6,2.9));
#6655=CARTESIAN_POINT('Origin',(1.6,32.,2.9));
#6656=CARTESIAN_POINT('Origin',(1.6,32.,2.9));
#6657=CARTESIAN_POINT('',(1.9,32.4,2.9));
#6658=CARTESIAN_POINT('',(1.9,32.4,6.5));
#6659=CARTESIAN_POINT('',(1.9,32.4,2.9));
#6660=CARTESIAN_POINT('',(1.9,31.6,2.9));
#6661=CARTESIAN_POINT('Origin',(1.6,32.,2.9));
#6662=CARTESIAN_POINT('',(1.9,31.6,6.5));
#6663=CARTESIAN_POINT('',(1.9,31.6,2.9));
#6664=CARTESIAN_POINT('Origin',(1.6,32.,6.5));
#6665=CARTESIAN_POINT('Origin',(1.6,32.,2.9));
#6666=CARTESIAN_POINT('',(3.3,32.4,2.9));
#6667=CARTESIAN_POINT('',(1.3,31.6,2.9));
#6668=CARTESIAN_POINT('',(1.325,32.,2.9));
#6669=CARTESIAN_POINT('Origin',(1.6,32.,2.9));
#6670=CARTESIAN_POINT('Origin',(4.4,32.,2.9));
#6671=CARTESIAN_POINT('',(4.1,32.4,6.5));
#6672=CARTESIAN_POINT('',(4.1,32.4,2.9));
#6673=CARTESIAN_POINT('',(4.1,32.4,2.9));
#6674=CARTESIAN_POINT('',(4.1,31.6,6.5));
#6675=CARTESIAN_POINT('Origin',(4.4,32.,6.5));
#6676=CARTESIAN_POINT('',(4.1,31.6,2.9));
#6677=CARTESIAN_POINT('',(4.1,31.6,2.9));
#6678=CARTESIAN_POINT('Origin',(4.4,32.,2.9));
#6679=CARTESIAN_POINT('Origin',(4.4,32.,2.9));
#6680=CARTESIAN_POINT('',(4.7,32.4,2.9));
#6681=CARTESIAN_POINT('',(4.7,32.4,6.5));
#6682=CARTESIAN_POINT('',(4.7,32.4,2.9));
#6683=CARTESIAN_POINT('',(4.7,31.6,2.9));
#6684=CARTESIAN_POINT('Origin',(4.4,32.,2.9));
#6685=CARTESIAN_POINT('',(4.7,31.6,6.5));
#6686=CARTESIAN_POINT('',(4.7,31.6,2.9));
#6687=CARTESIAN_POINT('Origin',(4.4,32.,6.5));
#6688=CARTESIAN_POINT('Origin',(4.4,32.,2.9));
#6689=CARTESIAN_POINT('',(4.7,32.4,2.9));
#6690=CARTESIAN_POINT('',(2.7,31.6,2.9));
#6691=CARTESIAN_POINT('',(4.125,32.,2.9));
#6692=CARTESIAN_POINT('Origin',(4.4,32.,2.9));
#6693=CARTESIAN_POINT('Origin',(1.,31.6,2.));
#6694=CARTESIAN_POINT('',(1.,31.6,6.5));
#6695=CARTESIAN_POINT('',(1.,31.6,6.5));
#6696=CARTESIAN_POINT('',(1.,31.6,2.8));
#6697=CARTESIAN_POINT('',(1.,31.6,2.));
#6698=CARTESIAN_POINT('',(5.,31.6,2.8));
#6699=CARTESIAN_POINT('',(1.,31.6,2.8));
#6700=CARTESIAN_POINT('',(5.,31.6,6.5));
#6701=CARTESIAN_POINT('',(5.,31.6,2.));
#6702=CARTESIAN_POINT('',(1.,31.6,6.5));
#6703=CARTESIAN_POINT('',(1.,31.6,6.5));
#6704=CARTESIAN_POINT('',(2.495,31.6,4.5));
#6705=CARTESIAN_POINT('Origin',(3.,31.6,4.5));
#6706=CARTESIAN_POINT('Origin',(3.,32.,6.5));
#6707=CARTESIAN_POINT('',(5.,32.4,6.5));
#6708=CARTESIAN_POINT('',(5.,31.6,6.5));
#6709=CARTESIAN_POINT('',(5.,32.4,6.5));
#6710=CARTESIAN_POINT('Origin',(3.,32.,6.5));
#6711=CARTESIAN_POINT('',(1.,32.4,6.5));
#6712=CARTESIAN_POINT('',(5.,32.4,6.5));
#6713=CARTESIAN_POINT('',(1.,32.4,6.5));
#6714=CARTESIAN_POINT('Origin',(3.,32.,6.5));
#6715=CARTESIAN_POINT('',(5.,32.4,6.5));
#6716=CARTESIAN_POINT('Origin',(1.6,32.,1.9));
#6717=CARTESIAN_POINT('',(1.325,32.,2.));
#6718=CARTESIAN_POINT('Origin',(1.6,32.,2.));
#6719=CARTESIAN_POINT('',(1.325,32.,1.9));
#6720=CARTESIAN_POINT('Origin',(4.4,32.,1.9));
#6721=CARTESIAN_POINT('',(4.125,32.,2.));
#6722=CARTESIAN_POINT('Origin',(4.4,32.,2.));
#6723=CARTESIAN_POINT('',(4.125,32.,1.9));
#6724=CARTESIAN_POINT('Origin',(3.,31.5,4.5));
#6725=CARTESIAN_POINT('',(2.495,32.4,4.5));
#6726=CARTESIAN_POINT('',(2.495,31.5,4.5));
#6727=CARTESIAN_POINT('Origin',(3.,32.4,4.5));
#6728=CARTESIAN_POINT('Origin',(1.,31.,2.8));
#6729=CARTESIAN_POINT('',(1.,31.,2.8));
#6730=CARTESIAN_POINT('',(1.,31.,2.8));
#6731=CARTESIAN_POINT('',(5.,31.,2.8));
#6732=CARTESIAN_POINT('',(5.,31.,2.8));
#6733=CARTESIAN_POINT('',(5.,31.,2.8));
#6734=CARTESIAN_POINT('Origin',(1.,31.,2.8));
#6735=CARTESIAN_POINT('',(5.,32.4,2.8));
#6736=CARTESIAN_POINT('',(1.,32.4,2.8));
#6737=CARTESIAN_POINT('',(3.,32.4,2.8));
#6738=CARTESIAN_POINT('',(5.,33.,2.8));
#6739=CARTESIAN_POINT('',(5.,31.,2.8));
#6740=CARTESIAN_POINT('',(1.,33.,2.8));
#6741=CARTESIAN_POINT('',(5.,33.,2.8));
#6742=CARTESIAN_POINT('',(1.,31.,2.8));
#6743=CARTESIAN_POINT('Origin',(3.,33.,2.4));
#6744=CARTESIAN_POINT('',(5.,33.,2.));
#6745=CARTESIAN_POINT('',(5.,33.,2.));
#6746=CARTESIAN_POINT('',(1.,33.,2.));
#6747=CARTESIAN_POINT('',(1.,33.,2.));
#6748=CARTESIAN_POINT('',(1.,33.,2.8));
#6749=CARTESIAN_POINT('Origin',(3.,31.,2.4));
#6750=CARTESIAN_POINT('',(1.,31.,2.));
#6751=CARTESIAN_POINT('',(1.,31.,2.8));
#6752=CARTESIAN_POINT('',(5.,31.,2.));
#6753=CARTESIAN_POINT('',(1.,31.,2.));
#6754=CARTESIAN_POINT('',(5.,31.,2.));
#6755=CARTESIAN_POINT('Origin',(5.,32.4,2.));
#6756=CARTESIAN_POINT('',(5.,32.4,2.));
#6757=CARTESIAN_POINT('',(1.,32.4,2.));
#6758=CARTESIAN_POINT('Origin',(1.,32.4,2.));
#6759=CARTESIAN_POINT('',(1.,32.4,2.));
#6760=CARTESIAN_POINT('Origin',(5.,31.6,2.));
#6761=CARTESIAN_POINT('',(5.,31.,2.));
#6762=CARTESIAN_POINT('Origin',(3.,32.,2.));
#7765=UNCERTAINTY_MEASURE_WITH_UNIT(LENGTH_MEASURE(0.001),#7807,
'DISTANCE_ACCURACY_VALUE',
'Maximum model space distance between geometric entities at asserted c
onnectivities');
#7782=UNCERTAINTY_MEASURE_WITH_UNIT(LENGTH_MEASURE(0.001),#7807,
'DISTANCE_ACCURACY_VALUE',
'Maximum model space distance between geometric entities at asserted c
onnectivities');
#7789=(
GEOMETRIC_REPRESENTATION_CONTEXT(3)
GLOBAL_UNCERTAINTY_ASSIGNED_CONTEXT((#7765))
GLOBAL_UNIT_ASSIGNED_CONTEXT((#7807,#7809,#7810))
REPRESENTATION_CONTEXT('','3D')
);
#7806=(
GEOMETRIC_REPRESENTATION_CONTEXT(3)
GLOBAL_UNCERTAINTY_ASSIGNED_CONTEXT((#7782))
GLOBAL_UNIT_ASSIGNED_CONTEXT((#7807,#7809,#7810))
REPRESENTATION_CONTEXT('','3D')
);
#7807=(
LENGTH_UNIT()
NAMED_UNIT(*)
SI_UNIT(.CENTI.,.METRE.)
);
#7809=(
NAMED_UNIT(*)
PLANE_ANGLE_UNIT()
SI_UNIT($,.RADIAN.)
);
#7810=(
NAMED_UNIT(*)
SI_UNIT($,.STERADIAN.)
SOLID_ANGLE_UNIT()
);
#7817=SHAPE_DEFINITION_REPRESENTATION(#7840,#7916);
#7840=PRODUCT_DEFINITION_SHAPE('',$,#7940);
#7916=SHAPE_REPRESENTATION('',(#4537),#7789);
#7933=PRODUCT_DEFINITION_CONTEXT('part definition',#8004,'design');
#7940=PRODUCT_DEFINITION('Axle Mount B','Axle Mount B',#7963,#7933);
#7963=PRODUCT_DEFINITION_FORMATION('',$,#8012);
#8004=APPLICATION_CONTEXT(
'Core Data for Automotive Mechanical Design Process');
#8005=PRODUCT_CONTEXT('part definition',#8004,'mechanical');
#8012=PRODUCT('Axle Mount B','Axle Mount B','Axle Mount B',
(#8005));
#8085=COLOUR_RGB('Grey',0.48,0.52,0.57);
#8086=FILL_AREA_STYLE_COLOUR('',#8085);
#8087=FILL_AREA_STYLE('',(#8086));
#8088=SURFACE_STYLE_FILL_AREA(#8087);
#8089=SURFACE_SIDE_STYLE('',(#8088));
#8090=SURFACE_STYLE_USAGE(.BOTH.,#8089);
#8091=PRESENTATION_STYLE_ASSIGNMENT((#8090));
ENDSEC;
END-ISO-10303-21;
